ISO-10303-21;
HEADER;
/* Generated by software containing ST-Developer
 * from STEP Tools, Inc. (www.steptools.com) 
 */

FILE_DESCRIPTION(
/* description */ ('Bin tilter linkage'),
/* implementation_level */ '2;1');

FILE_NAME(
/* name */ 'Bearing cap (4).step',
/* time_stamp */ '2026-10-28T03:26:24-07:00',
/* author */ (''),
/* organization */ (''),
/* preprocessor_version */ 'ST-DEVELOPER v20.2',
/* originating_system */ 'Autodesk Translation Framework v15.17.0.0',
/* authorisation */ '');

FILE_SCHEMA (('AUTOMOTIVE_DESIGN { 1 0 10303 214 3 1 1 }'));
ENDSEC;

DATA;
#10=MECHANICAL_DESIGN_GEOMETRIC_PRESENTATION_REPRESENTATION('',(#914),#23728);
#702=SHAPE_REPRESENTATION_RELATIONSHIP('SRR','None',#24168,#808);
#808=ADVANCED_BREP_SHAPE_REPRESENTATION('',(#1027),#23668);
#914=STYLED_ITEM('',(#24765),#1027);
#1027=MANIFOLD_SOLID_BREP('Body1',#12445);
#1330=FACE_BOUND('',#3310,.T.);
#1331=FACE_BOUND('',#3311,.T.);
#1332=FACE_BOUND('',#3312,.T.);
#1333=FACE_BOUND('',#3313,.T.);
#1334=FACE_BOUND('',#3314,.T.);
#1335=FACE_BOUND('',#3316,.T.);
#1336=FACE_BOUND('',#3317,.T.);
#1337=FACE_BOUND('',#3318,.T.);
#1338=FACE_BOUND('',#3319,.T.);
#1339=FACE_BOUND('',#3320,.T.);
#1681=PLANE('',#14548);
#1682=PLANE('',#14549);
#2283=FACE_OUTER_BOUND('',#3303,.T.);
#2284=FACE_OUTER_BOUND('',#3304,.T.);
#2285=FACE_OUTER_BOUND('',#3305,.T.);
#2286=FACE_OUTER_BOUND('',#3306,.T.);
#2287=FACE_OUTER_BOUND('',#3307,.T.);
#2288=FACE_OUTER_BOUND('',#3308,.T.);
#2289=FACE_OUTER_BOUND('',#3309,.T.);
#2290=FACE_OUTER_BOUND('',#3315,.T.);
#3303=EDGE_LOOP('',(#9877,#9878,#9879,#9880));
#3304=EDGE_LOOP('',(#9881,#9882,#9883,#9884));
#3305=EDGE_LOOP('',(#9885,#9886,#9887,#9888));
#3306=EDGE_LOOP('',(#9889,#9890,#9891,#9892));
#3307=EDGE_LOOP('',(#9893,#9894,#9895,#9896));
#3308=EDGE_LOOP('',(#9897,#9898,#9899,#9900));
#3309=EDGE_LOOP('',(#9901));
#3310=EDGE_LOOP('',(#9902));
#3311=EDGE_LOOP('',(#9903));
#3312=EDGE_LOOP('',(#9904));
#3313=EDGE_LOOP('',(#9905));
#3314=EDGE_LOOP('',(#9906));
#3315=EDGE_LOOP('',(#9907));
#3316=EDGE_LOOP('',(#9908));
#3317=EDGE_LOOP('',(#9909));
#3318=EDGE_LOOP('',(#9910));
#3319=EDGE_LOOP('',(#9911));
#3320=EDGE_LOOP('',(#9912));
#4197=LINE('',#21451,#4872);
#4198=LINE('',#21457,#4873);
#4199=LINE('',#21463,#4874);
#4200=LINE('',#21469,#4875);
#4201=LINE('',#21475,#4876);
#4202=LINE('',#21481,#4877);
#4872=VECTOR('',#17534,0.225000000000001);
#4873=VECTOR('',#17541,0.225000000000001);
#4874=VECTOR('',#17548,0.225000000000001);
#4875=VECTOR('',#17555,0.225000000000001);
#4876=VECTOR('',#17562,1.02);
#4877=VECTOR('',#17569,2.2);
#5603=CIRCLE('',#14531,0.225000000000001);
#5604=CIRCLE('',#14532,0.225000000000001);
#5605=CIRCLE('',#14534,0.225000000000001);
#5606=CIRCLE('',#14535,0.225000000000001);
#5607=CIRCLE('',#14537,0.225000000000001);
#5608=CIRCLE('',#14538,0.225000000000001);
#5609=CIRCLE('',#14540,0.225000000000001);
#5610=CIRCLE('',#14541,0.225000000000001);
#5611=CIRCLE('',#14543,1.02);
#5612=CIRCLE('',#14544,1.02);
#5613=CIRCLE('',#14546,2.2);
#5614=CIRCLE('',#14547,2.2);
#6457=VERTEX_POINT('',#21448);
#6458=VERTEX_POINT('',#21450);
#6459=VERTEX_POINT('',#21454);
#6460=VERTEX_POINT('',#21456);
#6461=VERTEX_POINT('',#21460);
#6462=VERTEX_POINT('',#21462);
#6463=VERTEX_POINT('',#21466);
#6464=VERTEX_POINT('',#21468);
#6465=VERTEX_POINT('',#21472);
#6466=VERTEX_POINT('',#21474);
#6467=VERTEX_POINT('',#21478);
#6468=VERTEX_POINT('',#21480);
#7678=EDGE_CURVE('',#6457,#6457,#5603,.T.);
#7679=EDGE_CURVE('',#6457,#6458,#4197,.T.);
#7680=EDGE_CURVE('',#6458,#6458,#5604,.T.);
#7681=EDGE_CURVE('',#6459,#6459,#5605,.T.);
#7682=EDGE_CURVE('',#6459,#6460,#4198,.T.);
#7683=EDGE_CURVE('',#6460,#6460,#5606,.T.);
#7684=EDGE_CURVE('',#6461,#6461,#5607,.T.);
#7685=EDGE_CURVE('',#6461,#6462,#4199,.T.);
#7686=EDGE_CURVE('',#6462,#6462,#5608,.T.);
#7687=EDGE_CURVE('',#6463,#6463,#5609,.T.);
#7688=EDGE_CURVE('',#6463,#6464,#4200,.T.);
#7689=EDGE_CURVE('',#6464,#6464,#5610,.T.);
#7690=EDGE_CURVE('',#6465,#6465,#5611,.T.);
#7691=EDGE_CURVE('',#6465,#6466,#4201,.T.);
#7692=EDGE_CURVE('',#6466,#6466,#5612,.T.);
#7693=EDGE_CURVE('',#6467,#6467,#5613,.T.);
#7694=EDGE_CURVE('',#6467,#6468,#4202,.T.);
#7695=EDGE_CURVE('',#6468,#6468,#5614,.T.);
#9877=ORIENTED_EDGE('',*,*,#7678,.F.);
#9878=ORIENTED_EDGE('',*,*,#7679,.T.);
#9879=ORIENTED_EDGE('',*,*,#7680,.F.);
#9880=ORIENTED_EDGE('',*,*,#7679,.F.);
#9881=ORIENTED_EDGE('',*,*,#7681,.F.);
#9882=ORIENTED_EDGE('',*,*,#7682,.T.);
#9883=ORIENTED_EDGE('',*,*,#7683,.F.);
#9884=ORIENTED_EDGE('',*,*,#7682,.F.);
#9885=ORIENTED_EDGE('',*,*,#7684,.F.);
#9886=ORIENTED_EDGE('',*,*,#7685,.T.);
#9887=ORIENTED_EDGE('',*,*,#7686,.F.);
#9888=ORIENTED_EDGE('',*,*,#7685,.F.);
#9889=ORIENTED_EDGE('',*,*,#7687,.F.);
#9890=ORIENTED_EDGE('',*,*,#7688,.T.);
#9891=ORIENTED_EDGE('',*,*,#7689,.F.);
#9892=ORIENTED_EDGE('',*,*,#7688,.F.);
#9893=ORIENTED_EDGE('',*,*,#7690,.F.);
#9894=ORIENTED_EDGE('',*,*,#7691,.T.);
#9895=ORIENTED_EDGE('',*,*,#7692,.T.);
#9896=ORIENTED_EDGE('',*,*,#7691,.F.);
#9897=ORIENTED_EDGE('',*,*,#7693,.F.);
#9898=ORIENTED_EDGE('',*,*,#7694,.T.);
#9899=ORIENTED_EDGE('',*,*,#7695,.T.);
#9900=ORIENTED_EDGE('',*,*,#7694,.F.);
#9901=ORIENTED_EDGE('',*,*,#7693,.T.);
#9902=ORIENTED_EDGE('',*,*,#7690,.T.);
#9903=ORIENTED_EDGE('',*,*,#7689,.T.);
#9904=ORIENTED_EDGE('',*,*,#7686,.T.);
#9905=ORIENTED_EDGE('',*,*,#7683,.T.);
#9906=ORIENTED_EDGE('',*,*,#7680,.T.);
#9907=ORIENTED_EDGE('',*,*,#7695,.F.);
#9908=ORIENTED_EDGE('',*,*,#7692,.F.);
#9909=ORIENTED_EDGE('',*,*,#7687,.T.);
#9910=ORIENTED_EDGE('',*,*,#7684,.T.);
#9911=ORIENTED_EDGE('',*,*,#7681,.T.);
#9912=ORIENTED_EDGE('',*,*,#7678,.T.);
#11467=CYLINDRICAL_SURFACE('',#14530,0.225000000000001);
#11468=CYLINDRICAL_SURFACE('',#14533,0.225000000000001);
#11469=CYLINDRICAL_SURFACE('',#14536,0.225000000000001);
#11470=CYLINDRICAL_SURFACE('',#14539,0.225000000000001);
#11471=CYLINDRICAL_SURFACE('',#14542,1.02);
#11472=CYLINDRICAL_SURFACE('',#14545,2.2);
#12008=ADVANCED_FACE('',(#2283),#11467,.F.);
#12009=ADVANCED_FACE('',(#2284),#11468,.F.);
#12010=ADVANCED_FACE('',(#2285),#11469,.F.);
#12011=ADVANCED_FACE('',(#2286),#11470,.F.);
#12012=ADVANCED_FACE('',(#2287),#11471,.F.);
#12013=ADVANCED_FACE('',(#2288),#11472,.T.);
#12014=ADVANCED_FACE('',(#2289,#1330,#1331,#1332,#1333,#1334),#1681,.T.);
#12015=ADVANCED_FACE('',(#2290,#1335,#1336,#1337,#1338,#1339),#1682,.F.);
#12445=CLOSED_SHELL('',(#12008,#12009,#12010,#12011,#12012,#12013,#12014,
#12015));
#14529=AXIS2_PLACEMENT_3D('',#21446,#17528,#17529);
#14530=AXIS2_PLACEMENT_3D('',#21447,#17530,#17531);
#14531=AXIS2_PLACEMENT_3D('',#21449,#17532,#17533);
#14532=AXIS2_PLACEMENT_3D('',#21452,#17535,#17536);
#14533=AXIS2_PLACEMENT_3D('',#21453,#17537,#17538);
#14534=AXIS2_PLACEMENT_3D('',#21455,#17539,#17540);
#14535=AXIS2_PLACEMENT_3D('',#21458,#17542,#17543);
#14536=AXIS2_PLACEMENT_3D('',#21459,#17544,#17545);
#14537=AXIS2_PLACEMENT_3D('',#21461,#17546,#17547);
#14538=AXIS2_PLACEMENT_3D('',#21464,#17549,#17550);
#14539=AXIS2_PLACEMENT_3D('',#21465,#17551,#17552);
#14540=AXIS2_PLACEMENT_3D('',#21467,#17553,#17554);
#14541=AXIS2_PLACEMENT_3D('',#21470,#17556,#17557);
#14542=AXIS2_PLACEMENT_3D('',#21471,#17558,#17559);
#14543=AXIS2_PLACEMENT_3D('',#21473,#17560,#17561);
#14544=AXIS2_PLACEMENT_3D('',#21476,#17563,#17564);
#14545=AXIS2_PLACEMENT_3D('',#21477,#17565,#17566);
#14546=AXIS2_PLACEMENT_3D('',#21479,#17567,#17568);
#14547=AXIS2_PLACEMENT_3D('',#21482,#17570,#17571);
#14548=AXIS2_PLACEMENT_3D('',#21483,#17572,#17573);
#14549=AXIS2_PLACEMENT_3D('',#21484,#17574,#17575);
#17528=DIRECTION('axis',(0.,0.,1.));
#17529=DIRECTION('refdir',(1.,0.,0.));
#17530=DIRECTION('center_axis',(0.,1.,0.));
#17531=DIRECTION('ref_axis',(1.,0.,0.));
#17532=DIRECTION('center_axis',(0.,1.,0.));
#17533=DIRECTION('ref_axis',(1.,0.,0.));
#17534=DIRECTION('',(0.,1.,0.));
#17535=DIRECTION('center_axis',(0.,-1.,0.));
#17536=DIRECTION('ref_axis',(1.,0.,0.));
#17537=DIRECTION('center_axis',(0.,1.,0.));
#17538=DIRECTION('ref_axis',(1.,0.,0.));
#17539=DIRECTION('center_axis',(0.,1.,0.));
#17540=DIRECTION('ref_axis',(1.,0.,0.));
#17541=DIRECTION('',(0.,1.,0.));
#17542=DIRECTION('center_axis',(0.,-1.,0.));
#17543=DIRECTION('ref_axis',(1.,0.,0.));
#17544=DIRECTION('center_axis',(0.,1.,0.));
#17545=DIRECTION('ref_axis',(1.,0.,0.));
#17546=DIRECTION('center_axis',(0.,1.,0.));
#17547=DIRECTION('ref_axis',(1.,0.,0.));
#17548=DIRECTION('',(0.,1.,0.));
#17549=DIRECTION('center_axis',(0.,-1.,0.));
#17550=DIRECTION('ref_axis',(1.,0.,0.));
#17551=DIRECTION('center_axis',(0.,1.,0.));
#17552=DIRECTION('ref_axis',(1.,0.,0.));
#17553=DIRECTION('center_axis',(0.,1.,0.));
#17554=DIRECTION('ref_axis',(1.,0.,0.));
#17555=DIRECTION('',(0.,1.,0.));
#17556=DIRECTION('center_axis',(0.,-1.,0.));
#17557=DIRECTION('ref_axis',(1.,0.,0.));
#17558=DIRECTION('center_axis',(0.,1.,0.));
#17559=DIRECTION('ref_axis',(1.,0.,0.));
#17560=DIRECTION('center_axis',(0.,-1.,0.));
#17561=DIRECTION('ref_axis',(1.,0.,0.));
#17562=DIRECTION('',(0.,-1.,0.));
#17563=DIRECTION('center_axis',(0.,-1.,0.));
#17564=DIRECTION('ref_axis',(1.,0.,0.));
#17565=DIRECTION('center_axis',(0.,1.,0.));
#17566=DIRECTION('ref_axis',(1.,0.,0.));
#17567=DIRECTION('center_axis',(0.,1.,0.));
#17568=DIRECTION('ref_axis',(1.,0.,0.));
#17569=DIRECTION('',(0.,-1.,0.));
#17570=DIRECTION('center_axis',(0.,1.,0.));
#17571=DIRECTION('ref_axis',(1.,0.,0.));
#17572=DIRECTION('center_axis',(0.,1.,0.));
#17573=DIRECTION('ref_axis',(1.,0.,0.));
#17574=DIRECTION('center_axis',(0.,1.,0.));
#17575=DIRECTION('ref_axis',(1.,0.,0.));
#21446=CARTESIAN_POINT('',(0.,0.,0.));
#21447=CARTESIAN_POINT('Origin',(16.6918524548049,-0.9,13.6918524548049));
#21448=CARTESIAN_POINT('',(16.4668524548049,-0.8,13.6918524548049));
#21449=CARTESIAN_POINT('Origin',(16.6918524548049,-0.8,13.6918524548049));
#21450=CARTESIAN_POINT('',(16.4668524548049,-0.5,13.6918524548049));
#21451=CARTESIAN_POINT('',(16.4668524548049,-0.9,13.6918524548049));
#21452=CARTESIAN_POINT('Origin',(16.6918524548049,-0.5,13.6918524548049));
#21453=CARTESIAN_POINT('Origin',(16.6918524548049,-0.9,16.3081475451951));
#21454=CARTESIAN_POINT('',(16.4668524548049,-0.8,16.3081475451951));
#21455=CARTESIAN_POINT('Origin',(16.6918524548049,-0.8,16.3081475451951));
#21456=CARTESIAN_POINT('',(16.4668524548049,-0.5,16.3081475451951));
#21457=CARTESIAN_POINT('',(16.4668524548049,-0.9,16.3081475451951));
#21458=CARTESIAN_POINT('Origin',(16.6918524548049,-0.5,16.3081475451951));
#21459=CARTESIAN_POINT('Origin',(19.3081475451951,-0.9,16.3081475451951));
#21460=CARTESIAN_POINT('',(19.0831475451951,-0.8,16.3081475451951));
#21461=CARTESIAN_POINT('Origin',(19.3081475451951,-0.8,16.3081475451951));
#21462=CARTESIAN_POINT('',(19.0831475451951,-0.5,16.3081475451951));
#21463=CARTESIAN_POINT('',(19.0831475451951,-0.9,16.3081475451951));
#21464=CARTESIAN_POINT('Origin',(19.3081475451951,-0.5,16.3081475451951));
#21465=CARTESIAN_POINT('Origin',(19.3081475451951,-0.9,13.6918524548049));
#21466=CARTESIAN_POINT('',(19.0831475451951,-0.8,13.6918524548049));
#21467=CARTESIAN_POINT('Origin',(19.3081475451951,-0.8,13.6918524548049));
#21468=CARTESIAN_POINT('',(19.0831475451951,-0.5,13.6918524548049));
#21469=CARTESIAN_POINT('',(19.0831475451951,-0.9,13.6918524548049));
#21470=CARTESIAN_POINT('Origin',(19.3081475451951,-0.5,13.6918524548049));
#21471=CARTESIAN_POINT('Origin',(18.,-0.8,15.));
#21472=CARTESIAN_POINT('',(16.98,-0.5,15.));
#21473=CARTESIAN_POINT('Origin',(18.,-0.5,15.));
#21474=CARTESIAN_POINT('',(16.98,-0.8,15.));
#21475=CARTESIAN_POINT('',(16.98,-0.8,15.));
#21476=CARTESIAN_POINT('Origin',(18.,-0.8,15.));
#21477=CARTESIAN_POINT('Origin',(18.,-0.8,15.));
#21478=CARTESIAN_POINT('',(15.8,-0.5,15.));
#21479=CARTESIAN_POINT('Origin',(18.,-0.5,15.));
#21480=CARTESIAN_POINT('',(15.8,-0.8,15.));
#21481=CARTESIAN_POINT('',(15.8,-0.8,15.));
#21482=CARTESIAN_POINT('Origin',(18.,-0.8,15.));
#21483=CARTESIAN_POINT('Origin',(18.,-0.5,15.));
#21484=CARTESIAN_POINT('Origin',(18.,-0.8,15.));
#23551=UNCERTAINTY_MEASURE_WITH_UNIT(LENGTH_MEASURE(0.001),#23729,
'DISTANCE_ACCURACY_VALUE',
'Maximum model space distance between geometric entities at asserted c
onnectivities');
#23611=UNCERTAINTY_MEASURE_WITH_UNIT(LENGTH_MEASURE(0.001),#23729,
'DISTANCE_ACCURACY_VALUE',
'Maximum model space distance between geometric entities at asserted c
onnectivities');
#23668=(
GEOMETRIC_REPRESENTATION_CONTEXT(3)
GLOBAL_UNCERTAINTY_ASSIGNED_CONTEXT((#23551))
GLOBAL_UNIT_ASSIGNED_CONTEXT((#23729,#23731,#23732))
REPRESENTATION_CONTEXT('','3D')
);
#23728=(
GEOMETRIC_REPRESENTATION_CONTEXT(3)
GLOBAL_UNCERTAINTY_ASSIGNED_CONTEXT((#23611))
GLOBAL_UNIT_ASSIGNED_CONTEXT((#23729,#23731,#23732))
REPRESENTATION_CONTEXT('','3D')
);
#23729=(
LENGTH_UNIT()
NAMED_UNIT(*)
SI_UNIT(.CENTI.,.METRE.)
);
#23731=(
NAMED_UNIT(*)
PLANE_ANGLE_UNIT()
SI_UNIT($,.RADIAN.)
);
#23732=(
NAMED_UNIT(*)
SI_UNIT($,.STERADIAN.)
SOLID_ANGLE_UNIT()
);
#23789=SHAPE_DEFINITION_REPRESENTATION(#23905,#24168);
#23905=PRODUCT_DEFINITION_SHAPE('',$,#24285);
#24168=SHAPE_REPRESENTATION('',(#14529),#23668);
#24228=PRODUCT_DEFINITION_CONTEXT('part definition',#24578,'design');
#24285=PRODUCT_DEFINITION('Bearing cap (4)','Bearing cap (4)',#24401,#24228);
#24401=PRODUCT_DEFINITION_FORMATION('',$,#24636);
#24578=APPLICATION_CONTEXT(
'Core Data for Automotive Mechanical Design Process');
#24579=PRODUCT_CONTEXT('part definition',#24578,'mechanical');
#24636=PRODUCT('Bearing cap (4)','Bearing cap (4)','Bearing cap (4)',(#24579));
#24759=COLOUR_RGB('Grey',0.48,0.52,0.57);
#24760=FILL_AREA_STYLE_COLOUR('',#24759);
#24761=FILL_AREA_STYLE('',(#24760));
#24762=SURFACE_STYLE_FILL_AREA(#24761);
#24763=SURFACE_SIDE_STYLE('',(#24762));
#24764=SURFACE_STYLE_USAGE(.BOTH.,#24763);
#24765=PRESENTATION_STYLE_ASSIGNMENT((#24764));
ENDSEC;
END-ISO-10303-21;
